ISO-10303-21;
HEADER;
/* Generated by software containing ST-Developer
 * from STEP Tools, Inc. (www.steptools.com) 
 */

FILE_DESCRIPTION(
/* description */ (''),
/* implementation_level */ '2;1');

FILE_NAME(
/* name */ 'Pin_04.step',
/* time_stamp */ '2026-10-04T12:17:52-07:00',
/* author */ (''),
/* organization */ (''),
/* preprocessor_version */ 'ST-DEVELOPER v20.2',
/* originating_system */ 'Autodesk Translation Framework v15.15.0.0',
/* authorisation */ '');

FILE_SCHEMA (('AUTOMOTIVE_DESIGN { 1 0 10303 214 3 1 1 }'));
ENDSEC;

DATA;
#10=MECHANICAL_DESIGN_GEOMETRIC_PRESENTATION_REPRESENTATION('',(#69),#1602);
#53=SHAPE_REPRESENTATION_RELATIONSHIP('SRR','None',#1640,#61);
#61=ADVANCED_BREP_SHAPE_REPRESENTATION('',(#77),#1600);
#69=STYLED_ITEM('',(#1684),#77);
#77=MANIFOLD_SOLID_BREP('Body1',#780);
#127=CIRCLE('',#954,4.);
#128=CIRCLE('',#955,4.);
#152=CYLINDRICAL_SURFACE('',#953,4.);
#195=FACE_OUTER_BOUND('',#254,.T.);
#196=FACE_OUTER_BOUND('',#255,.T.);
#197=FACE_OUTER_BOUND('',#256,.T.);
#254=EDGE_LOOP('',(#684,#685,#686,#687));
#255=EDGE_LOOP('',(#688));
#256=EDGE_LOOP('',(#689));
#309=LINE('',#1556,#358);
#358=VECTOR('',#1189,4.);
#417=VERTEX_POINT('',#1553);
#418=VERTEX_POINT('',#1555);
#507=EDGE_CURVE('',#417,#417,#127,.T.);
#508=EDGE_CURVE('',#417,#418,#309,.T.);
#509=EDGE_CURVE('',#418,#418,#128,.T.);
#684=ORIENTED_EDGE('',*,*,#507,.F.);
#685=ORIENTED_EDGE('',*,*,#508,.T.);
#686=ORIENTED_EDGE('',*,*,#509,.T.);
#687=ORIENTED_EDGE('',*,*,#508,.F.);
#688=ORIENTED_EDGE('',*,*,#507,.T.);
#689=ORIENTED_EDGE('',*,*,#509,.F.);
#723=PLANE('',#956);
#724=PLANE('',#957);
#767=ADVANCED_FACE('',(#195),#152,.T.);
#768=ADVANCED_FACE('',(#196),#723,.T.);
#769=ADVANCED_FACE('',(#197),#724,.F.);
#780=CLOSED_SHELL('',(#767,#768,#769));
#952=AXIS2_PLACEMENT_3D('',#1551,#1183,#1184);
#953=AXIS2_PLACEMENT_3D('',#1552,#1185,#1186);
#954=AXIS2_PLACEMENT_3D('',#1554,#1187,#1188);
#955=AXIS2_PLACEMENT_3D('',#1557,#1190,#1191);
#956=AXIS2_PLACEMENT_3D('',#1558,#1192,#1193);
#957=AXIS2_PLACEMENT_3D('',#1559,#1194,#1195);
#1183=DIRECTION('axis',(0.,0.,1.));
#1184=DIRECTION('refdir',(1.,0.,0.));
#1185=DIRECTION('center_axis',(0.,1.,0.));
#1186=DIRECTION('ref_axis',(-1.,0.,0.));
#1187=DIRECTION('center_axis',(0.,1.,0.));
#1188=DIRECTION('ref_axis',(-1.,0.,0.));
#1189=DIRECTION('',(0.,-1.,0.));
#1190=DIRECTION('center_axis',(0.,1.,0.));
#1191=DIRECTION('ref_axis',(-1.,0.,0.));
#1192=DIRECTION('center_axis',(0.,1.,0.));
#1193=DIRECTION('ref_axis',(-1.,0.,0.));
#1194=DIRECTION('center_axis',(0.,1.,0.));
#1195=DIRECTION('ref_axis',(-1.,0.,0.));
#1551=CARTESIAN_POINT('',(0.,0.,0.));
#1552=CARTESIAN_POINT('Origin',(23.8627874897787,0.,50.));
#1553=CARTESIAN_POINT('',(27.8627874897787,5.9999998808,50.));
#1554=CARTESIAN_POINT('Origin',(23.8627874897787,5.9999998808,50.));
#1555=CARTESIAN_POINT('',(27.8627874897787,-3.,50.));
#1556=CARTESIAN_POINT('',(27.8627874897787,0.,50.));
#1557=CARTESIAN_POINT('Origin',(23.8627874897787,-3.,50.));
#1558=CARTESIAN_POINT('Origin',(23.8627874897787,5.9999998808,50.));
#1559=CARTESIAN_POINT('Origin',(23.8627874897787,-3.,50.));
#1590=UNCERTAINTY_MEASURE_WITH_UNIT(LENGTH_MEASURE(0.01),#1603,
'DISTANCE_ACCURACY_VALUE',
'Maximum model space distance between geometric entities at asserted c
onnectivities');
#1592=UNCERTAINTY_MEASURE_WITH_UNIT(LENGTH_MEASURE(0.01),#1603,
'DISTANCE_ACCURACY_VALUE',
'Maximum model space distance between geometric entities at asserted c
onnectivities');
#1600=(
GEOMETRIC_REPRESENTATION_CONTEXT(3)
GLOBAL_UNCERTAINTY_ASSIGNED_CONTEXT((#1590))
GLOBAL_UNIT_ASSIGNED_CONTEXT((#1603,#1605,#1606))
REPRESENTATION_CONTEXT('','3D')
);
#1602=(
GEOMETRIC_REPRESENTATION_CONTEXT(3)
GLOBAL_UNCERTAINTY_ASSIGNED_CONTEXT((#1592))
GLOBAL_UNIT_ASSIGNED_CONTEXT((#1603,#1605,#1606))
REPRESENTATION_CONTEXT('','3D')
);
#1603=(
LENGTH_UNIT()
NAMED_UNIT(*)
SI_UNIT(.MILLI.,.METRE.)
);
#1605=(
NAMED_UNIT(*)
PLANE_ANGLE_UNIT()
SI_UNIT($,.RADIAN.)
);
#1606=(
NAMED_UNIT(*)
SI_UNIT($,.STERADIAN.)
SOLID_ANGLE_UNIT()
);
#1614=SHAPE_DEFINITION_REPRESENTATION(#1623,#1640);
#1623=PRODUCT_DEFINITION_SHAPE('',$,#1650);
#1640=SHAPE_REPRESENTATION('',(#952),#1600);
#1642=PRODUCT_DEFINITION_CONTEXT('part definition',#1671,'design');
#1650=PRODUCT_DEFINITION('Pin_04','Pin_04',#1659,#1642);
#1659=PRODUCT_DEFINITION_FORMATION('',$,#1680);
#1671=APPLICATION_CONTEXT(
'Core Data for Automotive Mechanical Design Process');
#1672=PRODUCT_CONTEXT('part definition',#1671,'mechanical');
#1680=PRODUCT('Pin_04','Pin_04',$,(#1672));
#1684=PRESENTATION_STYLE_ASSIGNMENT((#1688));
#1688=SURFACE_STYLE_USAGE(.BOTH.,#1692);
#1692=SURFACE_SIDE_STYLE('',(#1696));
#1696=SURFACE_STYLE_FILL_AREA(#1700);
#1700=FILL_AREA_STYLE('Opaque(160,160,160)',(#1704));
#1704=FILL_AREA_STYLE_COLOUR('Opaque(160,160,160)',#1708);
#1708=COLOUR_RGB('Opaque(160,160,160)', 0.66274510, 0.83137255, 0.94901961);
ENDSEC;
END-ISO-10303-21;
